ISO-10303-21;
HEADER;
/* Generated by software containing ST-Developer
 * from STEP Tools, Inc. (www.steptools.com) 
 */

FILE_DESCRIPTION(
/* description */ ('Chain-less indexing wheel (Geneva) drive'),
/* implementation_level */ '2;1');

FILE_NAME(
/* name */ 'Lower bearing sleeve (1).step',
/* time_stamp */ '2026-10-28T03:25:22-07:00',
/* author */ (''),
/* organization */ (''),
/* preprocessor_version */ 'ST-DEVELOPER v20.2',
/* originating_system */ 'Autodesk Translation Framework v15.17.0.0',
/* authorisation */ '');

FILE_SCHEMA (('AUTOMOTIVE_DESIGN { 1 0 10303 214 3 1 1 }'));
ENDSEC;

DATA;
#10=MECHANICAL_DESIGN_GEOMETRIC_PRESENTATION_REPRESENTATION('',(#333),#10957);
#275=SHAPE_REPRESENTATION_RELATIONSHIP('SRR','None',#11091,#300);
#300=ADVANCED_BREP_SHAPE_REPRESENTATION('',(#364),#10954);
#333=STYLED_ITEM('',(#11287),#364);
#364=MANIFOLD_SOLID_BREP('Body1',#5731);
#465=FACE_BOUND('',#1394,.T.);
#466=FACE_BOUND('',#1396,.T.);
#635=PLANE('',#6695);
#636=PLANE('',#6696);
#960=FACE_OUTER_BOUND('',#1391,.T.);
#961=FACE_OUTER_BOUND('',#1392,.T.);
#962=FACE_OUTER_BOUND('',#1393,.T.);
#963=FACE_OUTER_BOUND('',#1395,.T.);
#1391=EDGE_LOOP('',(#5127,#5128,#5129,#5130));
#1392=EDGE_LOOP('',(#5131,#5132,#5133,#5134));
#1393=EDGE_LOOP('',(#5135));
#1394=EDGE_LOOP('',(#5136));
#1395=EDGE_LOOP('',(#5137));
#1396=EDGE_LOOP('',(#5138));
#1765=LINE('',#10638,#2139);
#1766=LINE('',#10644,#2140);
#2139=VECTOR('',#8453,0.505);
#2140=VECTOR('',#8460,0.7);
#2489=CIRCLE('',#6690,0.505);
#2490=CIRCLE('',#6691,0.505);
#2491=CIRCLE('',#6693,0.7);
#2492=CIRCLE('',#6694,0.7);
#2961=VERTEX_POINT('',#10635);
#2962=VERTEX_POINT('',#10637);
#2963=VERTEX_POINT('',#10641);
#2964=VERTEX_POINT('',#10643);
#3689=EDGE_CURVE('',#2961,#2961,#2489,.T.);
#3690=EDGE_CURVE('',#2961,#2962,#1765,.T.);
#3691=EDGE_CURVE('',#2962,#2962,#2490,.T.);
#3692=EDGE_CURVE('',#2963,#2963,#2491,.T.);
#3693=EDGE_CURVE('',#2963,#2964,#1766,.T.);
#3694=EDGE_CURVE('',#2964,#2964,#2492,.T.);
#5127=ORIENTED_EDGE('',*,*,#3689,.F.);
#5128=ORIENTED_EDGE('',*,*,#3690,.T.);
#5129=ORIENTED_EDGE('',*,*,#3691,.T.);
#5130=ORIENTED_EDGE('',*,*,#3690,.F.);
#5131=ORIENTED_EDGE('',*,*,#3692,.F.);
#5132=ORIENTED_EDGE('',*,*,#3693,.T.);
#5133=ORIENTED_EDGE('',*,*,#3694,.T.);
#5134=ORIENTED_EDGE('',*,*,#3693,.F.);
#5135=ORIENTED_EDGE('',*,*,#3692,.T.);
#5136=ORIENTED_EDGE('',*,*,#3689,.T.);
#5137=ORIENTED_EDGE('',*,*,#3694,.F.);
#5138=ORIENTED_EDGE('',*,*,#3691,.F.);
#5359=CYLINDRICAL_SURFACE('',#6689,0.505);
#5360=CYLINDRICAL_SURFACE('',#6692,0.7);
#5674=ADVANCED_FACE('',(#960),#5359,.F.);
#5675=ADVANCED_FACE('',(#961),#5360,.T.);
#5676=ADVANCED_FACE('',(#962,#465),#635,.T.);
#5677=ADVANCED_FACE('',(#963,#466),#636,.F.);
#5731=CLOSED_SHELL('',(#5674,#5675,#5676,#5677));
#6688=AXIS2_PLACEMENT_3D('',#10633,#8447,#8448);
#6689=AXIS2_PLACEMENT_3D('',#10634,#8449,#8450);
#6690=AXIS2_PLACEMENT_3D('',#10636,#8451,#8452);
#6691=AXIS2_PLACEMENT_3D('',#10639,#8454,#8455);
#6692=AXIS2_PLACEMENT_3D('',#10640,#8456,#8457);
#6693=AXIS2_PLACEMENT_3D('',#10642,#8458,#8459);
#6694=AXIS2_PLACEMENT_3D('',#10645,#8461,#8462);
#6695=AXIS2_PLACEMENT_3D('',#10646,#8463,#8464);
#6696=AXIS2_PLACEMENT_3D('',#10647,#8465,#8466);
#8447=DIRECTION('axis',(0.,0.,1.));
#8448=DIRECTION('refdir',(1.,0.,0.));
#8449=DIRECTION('center_axis',(0.,0.,1.));
#8450=DIRECTION('ref_axis',(1.,0.,0.));
#8451=DIRECTION('center_axis',(0.,0.,-1.));
#8452=DIRECTION('ref_axis',(1.,0.,0.));
#8453=DIRECTION('',(0.,0.,-1.));
#8454=DIRECTION('center_axis',(0.,0.,-1.));
#8455=DIRECTION('ref_axis',(1.,0.,0.));
#8456=DIRECTION('center_axis',(0.,0.,1.));
#8457=DIRECTION('ref_axis',(1.,0.,0.));
#8458=DIRECTION('center_axis',(0.,0.,1.));
#8459=DIRECTION('ref_axis',(1.,0.,0.));
#8460=DIRECTION('',(0.,0.,-1.));
#8461=DIRECTION('center_axis',(0.,0.,1.));
#8462=DIRECTION('ref_axis',(1.,0.,0.));
#8463=DIRECTION('center_axis',(0.,0.,1.));
#8464=DIRECTION('ref_axis',(1.,0.,0.));
#8465=DIRECTION('center_axis',(0.,0.,1.));
#8466=DIRECTION('ref_axis',(1.,0.,0.));
#10633=CARTESIAN_POINT('',(0.,0.,0.));
#10634=CARTESIAN_POINT('Origin',(4.24264068711929,0.,1.8));
#10635=CARTESIAN_POINT('',(3.73764068711929,-6.18446633569413E-17,2.05));
#10636=CARTESIAN_POINT('Origin',(4.24264068711929,0.,2.05));
#10637=CARTESIAN_POINT('',(3.73764068711929,-6.18446633569413E-17,1.8));
#10638=CARTESIAN_POINT('',(3.73764068711929,-6.18446633569413E-17,1.8));
#10639=CARTESIAN_POINT('Origin',(4.24264068711929,0.,1.8));
#10640=CARTESIAN_POINT('Origin',(4.24264068711929,0.,1.8));
#10641=CARTESIAN_POINT('',(3.54264068711929,-8.57252759403147E-17,2.05));
#10642=CARTESIAN_POINT('Origin',(4.24264068711929,0.,2.05));
#10643=CARTESIAN_POINT('',(3.54264068711929,-8.57252759403147E-17,1.8));
#10644=CARTESIAN_POINT('',(3.54264068711929,-8.57252759403147E-17,1.8));
#10645=CARTESIAN_POINT('Origin',(4.24264068711929,0.,1.8));
#10646=CARTESIAN_POINT('Origin',(4.24264068711929,0.,2.05));
#10647=CARTESIAN_POINT('Origin',(4.24264068711929,0.,1.8));
#10923=UNCERTAINTY_MEASURE_WITH_UNIT(LENGTH_MEASURE(0.001),#10958,
'DISTANCE_ACCURACY_VALUE',
'Maximum model space distance between geometric entities at asserted c
onnectivities');
#10926=UNCERTAINTY_MEASURE_WITH_UNIT(LENGTH_MEASURE(0.001),#10958,
'DISTANCE_ACCURACY_VALUE',
'Maximum model space distance between geometric entities at asserted c
onnectivities');
#10954=(
GEOMETRIC_REPRESENTATION_CONTEXT(3)
GLOBAL_UNCERTAINTY_ASSIGNED_CONTEXT((#10923))
GLOBAL_UNIT_ASSIGNED_CONTEXT((#10958,#10960,#10961))
REPRESENTATION_CONTEXT('','3D')
);
#10957=(
GEOMETRIC_REPRESENTATION_CONTEXT(3)
GLOBAL_UNCERTAINTY_ASSIGNED_CONTEXT((#10926))
GLOBAL_UNIT_ASSIGNED_CONTEXT((#10958,#10960,#10961))
REPRESENTATION_CONTEXT('','3D')
);
#10958=(
LENGTH_UNIT()
NAMED_UNIT(*)
SI_UNIT(.CENTI.,.METRE.)
);
#10960=(
NAMED_UNIT(*)
PLANE_ANGLE_UNIT()
SI_UNIT($,.RADIAN.)
);
#10961=(
NAMED_UNIT(*)
SI_UNIT($,.STERADIAN.)
SOLID_ANGLE_UNIT()
);
#10989=SHAPE_DEFINITION_REPRESENTATION(#11044,#11091);
#11044=PRODUCT_DEFINITION_SHAPE('',$,#11122);
#11091=SHAPE_REPRESENTATION('',(#6688),#10954);
#11094=PRODUCT_DEFINITION_CONTEXT('part definition',#11186,'design');
#11122=PRODUCT_DEFINITION('Lower bearing sleeve (1)',
'Lower bearing sleeve (1)',#11152,#11094);
#11152=PRODUCT_DEFINITION_FORMATION('',$,#11215);
#11186=APPLICATION_CONTEXT(
'Core Data for Automotive Mechanical Design Process');
#11187=PRODUCT_CONTEXT('part definition',#11186,'mechanical');
#11215=PRODUCT('Lower bearing sleeve (1)','Lower bearing sleeve (1)',
'Lower bearing sleeve (1)',(#11187));
#11281=COLOUR_RGB('Grey',0.48,0.52,0.57);
#11282=FILL_AREA_STYLE_COLOUR('',#11281);
#11283=FILL_AREA_STYLE('',(#11282));
#11284=SURFACE_STYLE_FILL_AREA(#11283);
#11285=SURFACE_SIDE_STYLE('',(#11284));
#11286=SURFACE_STYLE_USAGE(.BOTH.,#11285);
#11287=PRESENTATION_STYLE_ASSIGNMENT((#11286));
ENDSEC;
END-ISO-10303-21;
